ISO-10303-21;
HEADER;
/* Generated by software containing ST-Developer
 * from STEP Tools, Inc. (www.steptools.com) 
 */
/* OPTION: using custom renumber hook */

FILE_DESCRIPTION(
/* description */ ('STEP AP242 Edition 2', 'CAx-IF Rec.Pracs.---Representation and Presentation of Product Manufa
cturing Information (PMI)---4.0---2014-10-13', 'CAx-IF Rec.Pracs.---3D Tessellated Geometry---0.4---2014-09-14', '2;1', 'CAx-IF Rec.Pracs.---User Defined Attributes---1.5---2016-08-15'),
/* implementation_level */ '2;1');

FILE_NAME(
/* name */ 'Part 3__PD10221.step',
/* time_stamp */ '2026-10-09T13:59:33Z',
/* author */ (''),
/* organization */ (''),
/* preprocessor_version */ 'ST-DEVELOPER v20',
/* originating_system */ 'ONSHAPE BY PTC INC, 1.221',
/* authorisation */ '  ');

FILE_SCHEMA (('AP242_MANAGED_MODEL_BASED_3D_ENGINEERING_MIM_LF { 1 0 10303 442 3 1 4 }'));
ENDSEC;

DATA;
#21=TOROIDAL_SURFACE('',#6377,0.05,0.0015);
#22=TOROIDAL_SURFACE('',#6383,0.05,0.0015);
#23=TOROIDAL_SURFACE('',#6391,0.05,0.0025);
#24=TOROIDAL_SURFACE('',#6396,0.05,0.0025);
#278=LINE('',#9843,#562);
#279=LINE('',#9847,#563);
#280=LINE('',#9861,#564);
#281=LINE('',#9862,#565);
#282=LINE('',#9873,#566);
#283=LINE('',#9883,#567);
#284=LINE('',#9888,#568);
#285=LINE('',#9892,#569);
#562=VECTOR('',#8104,1.);
#563=VECTOR('',#8107,1.);
#564=VECTOR('',#8116,1.);
#565=VECTOR('',#8117,1.);
#566=VECTOR('',#8120,1.);
#567=VECTOR('',#8121,1.);
#568=VECTOR('',#8126,1.);
#569=VECTOR('',#8129,1.);
#680=SHAPE_REPRESENTATION_RELATIONSHIP('','',#5699,#694);
#694=ADVANCED_BREP_SHAPE_REPRESENTATION('',(#5667),#10153);
#767=PLANE('',#6387);
#768=PLANE('',#6388);
#802=B_SPLINE_CURVE_WITH_KNOTS('',3,(#9833,#9834,#9835,#9836,#9837,#9838,
#9839),.UNSPECIFIED.,.F.,.F.,(4,1,1,1,4),(0.00864227471880883,0.00981748688955518,
0.0109926990603015,0.0121679112310479,0.0133431234017942),.UNSPECIFIED.);
#803=B_SPLINE_CURVE_WITH_KNOTS('',3,(#9853,#9854,#9855,#9856,#9857,#9858,
#9859),.UNSPECIFIED.,.F.,.F.,(4,1,1,1,4),(0.00546378704703531,0.00663876072579679,
0.00781373440455828,0.00898870808331976,0.0101636817620812),
 .UNSPECIFIED.);
#804=B_SPLINE_CURVE_WITH_KNOTS('',3,(#9864,#9865,#9866,#9867,#9868,#9869,
#9870),.UNSPECIFIED.,.F.,.F.,(4,1,1,1,4),(0.0142365147475521,0.0161947978067127,
0.0181530808658734,0.020111363925034,0.0220696469841946),.UNSPECIFIED.);
#805=B_SPLINE_CURVE_WITH_KNOTS('',3,(#9875,#9876,#9877,#9878,#9879,#9880,
#9881),.UNSPECIFIED.,.F.,.F.,(4,1,1,1,4),(0.00927377643444575,0.0112324591922964,
0.0131911419501471,0.0151498247079977,0.0171085074658484),.UNSPECIFIED.);
#2116=ORIENTED_EDGE('',*,*,#2995,.F.);
#2117=ORIENTED_EDGE('',*,*,#2996,.T.);
#2118=ORIENTED_EDGE('',*,*,#2997,.F.);
#2119=ORIENTED_EDGE('',*,*,#2998,.F.);
#2120=ORIENTED_EDGE('',*,*,#2999,.F.);
#2121=ORIENTED_EDGE('',*,*,#3000,.T.);
#2122=ORIENTED_EDGE('',*,*,#3001,.F.);
#2123=ORIENTED_EDGE('',*,*,#2996,.F.);
#2124=ORIENTED_EDGE('',*,*,#3002,.F.);
#2125=ORIENTED_EDGE('',*,*,#3003,.T.);
#2126=ORIENTED_EDGE('',*,*,#3004,.F.);
#2127=ORIENTED_EDGE('',*,*,#3000,.F.);
#2128=ORIENTED_EDGE('',*,*,#3005,.F.);
#2129=ORIENTED_EDGE('',*,*,#2998,.T.);
#2130=ORIENTED_EDGE('',*,*,#3006,.F.);
#2131=ORIENTED_EDGE('',*,*,#3003,.F.);
#2132=ORIENTED_EDGE('',*,*,#2997,.T.);
#2133=ORIENTED_EDGE('',*,*,#3001,.T.);
#2134=ORIENTED_EDGE('',*,*,#3004,.T.);
#2135=ORIENTED_EDGE('',*,*,#3006,.T.);
#2136=ORIENTED_EDGE('',*,*,#3007,.F.);
#2137=ORIENTED_EDGE('',*,*,#3008,.F.);
#2138=ORIENTED_EDGE('',*,*,#3009,.F.);
#2139=ORIENTED_EDGE('',*,*,#3010,.F.);
#2140=ORIENTED_EDGE('',*,*,#2995,.T.);
#2141=ORIENTED_EDGE('',*,*,#3005,.T.);
#2142=ORIENTED_EDGE('',*,*,#3002,.T.);
#2143=ORIENTED_EDGE('',*,*,#2999,.T.);
#2144=ORIENTED_EDGE('',*,*,#3011,.F.);
#2145=ORIENTED_EDGE('',*,*,#3012,.F.);
#2146=ORIENTED_EDGE('',*,*,#3013,.F.);
#2147=ORIENTED_EDGE('',*,*,#3014,.F.);
#2148=ORIENTED_EDGE('',*,*,#3011,.T.);
#2149=ORIENTED_EDGE('',*,*,#3015,.T.);
#2150=ORIENTED_EDGE('',*,*,#3007,.T.);
#2151=ORIENTED_EDGE('',*,*,#3016,.F.);
#2152=ORIENTED_EDGE('',*,*,#3017,.F.);
#2153=ORIENTED_EDGE('',*,*,#3012,.T.);
#2154=ORIENTED_EDGE('',*,*,#3016,.T.);
#2155=ORIENTED_EDGE('',*,*,#3010,.T.);
#2156=ORIENTED_EDGE('',*,*,#3013,.T.);
#2157=ORIENTED_EDGE('',*,*,#3017,.T.);
#2158=ORIENTED_EDGE('',*,*,#3009,.T.);
#2159=ORIENTED_EDGE('',*,*,#3018,.F.);
#2160=ORIENTED_EDGE('',*,*,#3015,.F.);
#2161=ORIENTED_EDGE('',*,*,#3014,.T.);
#2162=ORIENTED_EDGE('',*,*,#3018,.T.);
#2163=ORIENTED_EDGE('',*,*,#3008,.T.);
#2995=EDGE_CURVE('',#3565,#3566,#4046,.T.);
#2996=EDGE_CURVE('',#3565,#3567,#4047,.T.);
#2997=EDGE_CURVE('',#3568,#3567,#802,.T.);
#2998=EDGE_CURVE('',#3566,#3568,#4048,.T.);
#2999=EDGE_CURVE('',#3569,#3565,#278,.T.);
#3000=EDGE_CURVE('',#3569,#3570,#4049,.T.);
#3001=EDGE_CURVE('',#3567,#3570,#279,.F.);
#3002=EDGE_CURVE('',#3571,#3569,#4050,.T.);
#3003=EDGE_CURVE('',#3571,#3572,#4051,.T.);
#3004=EDGE_CURVE('',#3570,#3572,#803,.T.);
#3005=EDGE_CURVE('',#3566,#3571,#280,.F.);
#3006=EDGE_CURVE('',#3572,#3568,#281,.T.);
#3007=EDGE_CURVE('',#3573,#3574,#804,.T.);
#3008=EDGE_CURVE('',#3575,#3573,#282,.T.);
#3009=EDGE_CURVE('',#3576,#3575,#805,.T.);
#3010=EDGE_CURVE('',#3574,#3576,#283,.F.);
#3011=EDGE_CURVE('',#3577,#3578,#4052,.T.);
#3012=EDGE_CURVE('',#3579,#3577,#284,.T.);
#3013=EDGE_CURVE('',#3580,#3579,#4053,.T.);
#3014=EDGE_CURVE('',#3578,#3580,#285,.F.);
#3015=EDGE_CURVE('',#3578,#3573,#4054,.T.);
#3016=EDGE_CURVE('',#3577,#3574,#4055,.T.);
#3017=EDGE_CURVE('',#3579,#3576,#4056,.T.);
#3018=EDGE_CURVE('',#3580,#3575,#4057,.T.);
#3565=VERTEX_POINT('',#9829);
#3566=VERTEX_POINT('',#9830);
#3567=VERTEX_POINT('',#9832);
#3568=VERTEX_POINT('',#9840);
#3569=VERTEX_POINT('',#9844);
#3570=VERTEX_POINT('',#9846);
#3571=VERTEX_POINT('',#9850);
#3572=VERTEX_POINT('',#9852);
#3573=VERTEX_POINT('',#9871);
#3574=VERTEX_POINT('',#9872);
#3575=VERTEX_POINT('',#9874);
#3576=VERTEX_POINT('',#9882);
#3577=VERTEX_POINT('',#9886);
#3578=VERTEX_POINT('',#9887);
#3579=VERTEX_POINT('',#9889);
#3580=VERTEX_POINT('',#9891);
#4046=CIRCLE('',#6378,0.0015);
#4047=CIRCLE('',#6379,0.0485);
#4048=CIRCLE('',#6380,0.0515);
#4049=CIRCLE('',#6382,0.0485);
#4050=CIRCLE('',#6384,0.0015);
#4051=CIRCLE('',#6385,0.0515);
#4052=CIRCLE('',#6389,0.0025);
#4053=CIRCLE('',#6390,0.0025);
#4054=CIRCLE('',#6392,0.0525);
#4055=CIRCLE('',#6393,0.0475);
#4056=CIRCLE('',#6395,0.0475);
#4057=CIRCLE('',#6397,0.0525);
#4462=EDGE_LOOP('',(#2116,#2117,#2118,#2119));
#4463=EDGE_LOOP('',(#2120,#2121,#2122,#2123));
#4464=EDGE_LOOP('',(#2124,#2125,#2126,#2127));
#4465=EDGE_LOOP('',(#2128,#2129,#2130,#2131));
#4466=EDGE_LOOP('',(#2132,#2133,#2134,#2135));
#4467=EDGE_LOOP('',(#2136,#2137,#2138,#2139));
#4468=EDGE_LOOP('',(#2140,#2141,#2142,#2143));
#4469=EDGE_LOOP('',(#2144,#2145,#2146,#2147));
#4470=EDGE_LOOP('',(#2148,#2149,#2150,#2151));
#4471=EDGE_LOOP('',(#2152,#2153,#2154,#2155));
#4472=EDGE_LOOP('',(#2156,#2157,#2158,#2159));
#4473=EDGE_LOOP('',(#2160,#2161,#2162,#2163));
#4910=FACE_BOUND('',#4462,.T.);
#4911=FACE_BOUND('',#4463,.T.);
#4912=FACE_BOUND('',#4464,.T.);
#4913=FACE_BOUND('',#4465,.T.);
#4914=FACE_BOUND('',#4466,.T.);
#4915=FACE_BOUND('',#4467,.T.);
#4916=FACE_BOUND('',#4468,.T.);
#4917=FACE_BOUND('',#4469,.T.);
#4918=FACE_BOUND('',#4470,.T.);
#4919=FACE_BOUND('',#4471,.T.);
#4920=FACE_BOUND('',#4472,.T.);
#4921=FACE_BOUND('',#4473,.T.);
#5193=CYLINDRICAL_SURFACE('',#6381,0.0485);
#5194=CYLINDRICAL_SURFACE('',#6386,0.0515);
#5195=CYLINDRICAL_SURFACE('',#6394,0.0475);
#5196=CYLINDRICAL_SURFACE('',#6398,0.0525);
#5478=ADVANCED_FACE('',(#4910),#21,.F.);
#5479=ADVANCED_FACE('',(#4911),#5193,.T.);
#5480=ADVANCED_FACE('',(#4912),#22,.F.);
#5481=ADVANCED_FACE('',(#4913),#5194,.F.);
#5482=ADVANCED_FACE('',(#4914,#4915),#767,.F.);
#5483=ADVANCED_FACE('',(#4916,#4917),#768,.F.);
#5484=ADVANCED_FACE('',(#4918),#23,.T.);
#5485=ADVANCED_FACE('',(#4919),#5195,.F.);
#5486=ADVANCED_FACE('',(#4920),#24,.T.);
#5487=ADVANCED_FACE('',(#4921),#5196,.T.);
#5548=CLOSED_SHELL('',(#5478,#5479,#5480,#5481,#5482,#5483,#5484,#5485,
#5486,#5487));
#5562=STYLED_ITEM('',(#5576),#5667);
#5576=PRESENTATION_STYLE_ASSIGNMENT((#5590));
#5590=SURFACE_STYLE_USAGE(.BOTH.,#5604);
#5604=SURFACE_SIDE_STYLE('',(#5618));
#5618=SURFACE_STYLE_FILL_AREA(#5632);
#5632=FILL_AREA_STYLE('',(#5646));
#5646=FILL_AREA_STYLE_COLOUR('',#5656);
#5656=COLOUR_RGB('', 0.40784314, 0.44705882, 0.49803922);
#5667=MANIFOLD_SOLID_BREP('Part 3',#5548);
#5683=SHAPE_DEFINITION_REPRESENTATION(#10199,#5699);
#5699=SHAPE_REPRESENTATION('Part 3',(#5704),#10153);
#5704=AXIS2_PLACEMENT_3D('',#8391,#6505,#6506);
#6377=AXIS2_PLACEMENT_3D('',#9827,#8094,#8095);
#6378=AXIS2_PLACEMENT_3D('',#9828,#8096,#8097);
#6379=AXIS2_PLACEMENT_3D('',#9831,#8098,#8099);
#6380=AXIS2_PLACEMENT_3D('',#9841,#8100,#8101);
#6381=AXIS2_PLACEMENT_3D('',#9842,#8102,#8103);
#6382=AXIS2_PLACEMENT_3D('',#9845,#8105,#8106);
#6383=AXIS2_PLACEMENT_3D('',#9848,#8108,#8109);
#6384=AXIS2_PLACEMENT_3D('',#9849,#8110,#8111);
#6385=AXIS2_PLACEMENT_3D('',#9851,#8112,#8113);
#6386=AXIS2_PLACEMENT_3D('',#9860,#8114,#8115);
#6387=AXIS2_PLACEMENT_3D('',#9863,#8118,#8119);
#6388=AXIS2_PLACEMENT_3D('',#9884,#8122,#8123);
#6389=AXIS2_PLACEMENT_3D('',#9885,#8124,#8125);
#6390=AXIS2_PLACEMENT_3D('',#9890,#8127,#8128);
#6391=AXIS2_PLACEMENT_3D('',#9893,#8130,#8131);
#6392=AXIS2_PLACEMENT_3D('',#9894,#8132,#8133);
#6393=AXIS2_PLACEMENT_3D('',#9895,#8134,#8135);
#6394=AXIS2_PLACEMENT_3D('',#9896,#8136,#8137);
#6395=AXIS2_PLACEMENT_3D('',#9897,#8138,#8139);
#6396=AXIS2_PLACEMENT_3D('',#9898,#8140,#8141);
#6397=AXIS2_PLACEMENT_3D('',#9899,#8142,#8143);
#6398=AXIS2_PLACEMENT_3D('',#9900,#8144,#8145);
#6505=DIRECTION('',(0.,0.,1.));
#6506=DIRECTION('',(1.,0.,0.));
#8094=DIRECTION('',(-1.,0.,0.));
#8095=DIRECTION('',(0.,0.,1.));
#8096=DIRECTION('',(0.,1.27620930369834E-17,1.));
#8097=DIRECTION('',(0.,-1.,1.27620930369834E-17));
#8098=DIRECTION('',(-1.,0.,0.));
#8099=DIRECTION('',(0.,0.,1.));
#8100=DIRECTION('',(-1.,0.,0.));
#8101=DIRECTION('',(0.,0.,1.));
#8102=DIRECTION('',(-1.,0.,0.));
#8103=DIRECTION('',(0.,0.,1.));
#8104=DIRECTION('',(-1.,0.,0.));
#8105=DIRECTION('',(-1.,0.,0.));
#8106=DIRECTION('',(0.,0.,1.));
#8107=DIRECTION('',(-1.,0.,0.));
#8108=DIRECTION('',(-1.,0.,0.));
#8109=DIRECTION('',(0.,0.,1.));
#8110=DIRECTION('',(0.,1.27620930369834E-17,1.));
#8111=DIRECTION('',(0.,-1.,1.27620930369834E-17));
#8112=DIRECTION('',(-1.,0.,0.));
#8113=DIRECTION('',(0.,0.,1.));
#8114=DIRECTION('',(-1.,0.,0.));
#8115=DIRECTION('',(0.,0.,1.));
#8116=DIRECTION('',(-1.,0.,0.));
#8117=DIRECTION('',(-1.,0.,0.));
#8118=DIRECTION('',(0.,1.,-1.12666127576541E-17));
#8119=DIRECTION('',(0.,1.12666127576541E-17,1.));
#8120=DIRECTION('',(-1.,0.,0.));
#8121=DIRECTION('',(-1.,0.,0.));
#8122=DIRECTION('',(0.,1.27620930369834E-17,1.));
#8123=DIRECTION('',(0.,-1.,1.27620930369834E-17));
#8124=DIRECTION('',(0.,1.27620930369834E-17,1.));
#8125=DIRECTION('',(0.,-1.,1.27620930369834E-17));
#8126=DIRECTION('',(-1.,0.,0.));
#8127=DIRECTION('',(0.,1.27620930369834E-17,1.));
#8128=DIRECTION('',(0.,-1.,1.27620930369834E-17));
#8129=DIRECTION('',(-1.,0.,0.));
#8130=DIRECTION('',(-1.,0.,0.));
#8131=DIRECTION('',(0.,0.,1.));
#8132=DIRECTION('',(-1.,0.,0.));
#8133=DIRECTION('',(0.,0.,1.));
#8134=DIRECTION('',(-1.,0.,0.));
#8135=DIRECTION('',(0.,0.,1.));
#8136=DIRECTION('',(-1.,0.,0.));
#8137=DIRECTION('',(0.,0.,1.));
#8138=DIRECTION('',(-1.,0.,0.));
#8139=DIRECTION('',(0.,0.,1.));
#8140=DIRECTION('',(-1.,0.,0.));
#8141=DIRECTION('',(0.,0.,1.));
#8142=DIRECTION('',(-1.,0.,0.));
#8143=DIRECTION('',(0.,0.,1.));
#8144=DIRECTION('',(-1.,0.,0.));
#8145=DIRECTION('',(0.,0.,1.));
#8391=CARTESIAN_POINT('',(0.,0.,0.));
#9827=CARTESIAN_POINT('',(-0.0025,0.,0.));
#9828=CARTESIAN_POINT('',(-0.0025,-0.05,6.38104651849169E-19));
#9829=CARTESIAN_POINT('',(-0.0025,-0.0485,-8.6757429628926E-20));
#9830=CARTESIAN_POINT('',(-0.0025,-0.0515,-4.84711505179759E-20));
#9831=CARTESIAN_POINT('',(-0.0025,0.,0.));
#9832=CARTESIAN_POINT('',(-0.0025,0.005,-0.0482415795761291));
#9833=CARTESIAN_POINT('',(-0.0025,0.005,-0.0512567068782223));
#9834=CARTESIAN_POINT('',(-0.00289537313791363,0.005,-0.0512567068782223));
#9835=CARTESIAN_POINT('',(-0.00367744748009773,0.005,-0.0509278560554984));
#9836=CARTESIAN_POINT('',(-0.0041616283571214,0.005,-0.0497471530643231));
#9837=CARTESIAN_POINT('',(-0.00367603360051941,0.005,-0.0485697710976327));
#9838=CARTESIAN_POINT('',(-0.00289360144208482,0.005,-0.0482415795761291));
#9839=CARTESIAN_POINT('',(-0.0025,0.005,-0.0482415795761291));
#9840=CARTESIAN_POINT('',(-0.0025,0.005,-0.0512567068782223));
#9841=CARTESIAN_POINT('',(-0.0025,0.,0.));
#9842=CARTESIAN_POINT('',(-0.0951557364069925,0.,0.));
#9843=CARTESIAN_POINT('',(-0.0951557364069925,-0.0485,-8.6757429628926E-20));
#9844=CARTESIAN_POINT('',(0.0025,-0.0485,6.18961512293694E-19));
#9845=CARTESIAN_POINT('',(0.0025,0.,0.));
#9846=CARTESIAN_POINT('',(0.0025,0.005,-0.0482415795761291));
#9847=CARTESIAN_POINT('',(-0.0951557364069925,0.005,-0.0482415795761291));
#9848=CARTESIAN_POINT('',(0.0025,0.,0.));
#9849=CARTESIAN_POINT('',(0.0025,-0.05,6.38104651849169E-19));
#9850=CARTESIAN_POINT('',(0.0025,-0.0515,-4.84711505179759E-20));
#9851=CARTESIAN_POINT('',(0.0025,0.,0.));
#9852=CARTESIAN_POINT('',(0.0025,0.005,-0.0512567068782223));
#9853=CARTESIAN_POINT('',(0.0025,0.005,-0.0482415795761291));
#9854=CARTESIAN_POINT('',(0.00289405455214165,0.005,-0.0482415795761291));
#9855=CARTESIAN_POINT('',(0.00367769277965407,0.005,-0.0485708711433478));
#9856=CARTESIAN_POINT('',(0.00416046967205458,0.005,-0.0497486705893407));
#9857=CARTESIAN_POINT('',(0.00368042750626719,0.005,-0.0509263588341051));
#9858=CARTESIAN_POINT('',(0.00289165153003374,0.005,-0.0512567068782223));
#9859=CARTESIAN_POINT('',(0.0025,0.005,-0.0512567068782223));
#9860=CARTESIAN_POINT('',(-0.0951557364069925,0.,0.));
#9861=CARTESIAN_POINT('',(-0.0951557364069925,-0.0515,-4.84711505179759E-20));
#9862=CARTESIAN_POINT('',(-0.0951557364069925,0.005,-0.0512567068782223));
#9863=CARTESIAN_POINT('',(-0.005,0.005,-7.69529407107537E-19));
#9864=CARTESIAN_POINT('',(-0.0025,0.005,-0.0522613624009172));
#9865=CARTESIAN_POINT('',(-0.00315874911763011,0.005,-0.0522613624009172));
#9866=CARTESIAN_POINT('',(-0.00446402043389959,0.005,-0.051711570220507));
#9867=CARTESIAN_POINT('',(-0.00526880926820208,0.005,-0.0497473158066496));
#9868=CARTESIAN_POINT('',(-0.00446073660632804,0.005,-0.0477820413045601));
#9869=CARTESIAN_POINT('',(-0.00315306096378925,0.005,-0.047236109069228));
#9870=CARTESIAN_POINT('',(-0.0025,0.005,-0.047236109069228));
#9871=CARTESIAN_POINT('',(-0.0025,0.005,-0.0522613624009172));
#9872=CARTESIAN_POINT('',(-0.0025,0.005,-0.047236109069228));
#9873=CARTESIAN_POINT('',(-0.0951557364069925,0.005,-0.0522613624009172));
#9874=CARTESIAN_POINT('',(0.0025,0.005,-0.0522613624009172));
#9875=CARTESIAN_POINT('',(0.0025,0.005,-0.047236109069228));
#9876=CARTESIAN_POINT('',(0.00316127281190909,0.005,-0.047236109069228));
#9877=CARTESIAN_POINT('',(0.00445940049784844,0.005,-0.0477845184982856));
#9878=CARTESIAN_POINT('',(0.0052689178838484,0.005,-0.049746449755392));
#9879=CARTESIAN_POINT('',(0.00446492217011694,0.005,-0.0517126600905919));
#9880=CARTESIAN_POINT('',(0.00315462463920908,0.005,-0.0522613624009172));
#9881=CARTESIAN_POINT('',(0.0025,0.005,-0.0522613624009172));
#9882=CARTESIAN_POINT('',(0.0025,0.005,-0.047236109069228));
#9883=CARTESIAN_POINT('',(-0.0951557364069925,0.005,-0.047236109069228));
#9884=CARTESIAN_POINT('',(-0.005,0.005,-7.69529407107537E-19));
#9885=CARTESIAN_POINT('',(-0.0025,-0.05,6.38104651849169E-19));
#9886=CARTESIAN_POINT('',(-0.0025,-0.0475,-9.95195226659094E-20));
#9887=CARTESIAN_POINT('',(-0.0025,-0.0525,-3.57090574809925E-20));
#9888=CARTESIAN_POINT('',(-0.0951557364069925,-0.0475,-9.95195226659094E-20));
#9889=CARTESIAN_POINT('',(0.0025,-0.0475,6.0619941925671E-19));
#9890=CARTESIAN_POINT('',(0.0025,-0.05,6.38104651849169E-19));
#9891=CARTESIAN_POINT('',(0.0025,-0.0525,-3.57090574809925E-20));
#9892=CARTESIAN_POINT('',(-0.0951557364069925,-0.0525,-3.57090574809925E-20));
#9893=CARTESIAN_POINT('',(-0.0025,0.,0.));
#9894=CARTESIAN_POINT('',(-0.0025,0.,0.));
#9895=CARTESIAN_POINT('',(-0.0025,0.,0.));
#9896=CARTESIAN_POINT('',(-0.0951557364069925,0.,0.));
#9897=CARTESIAN_POINT('',(0.0025,0.,0.));
#9898=CARTESIAN_POINT('',(0.0025,0.,0.));
#9899=CARTESIAN_POINT('',(0.0025,0.,0.));
#9900=CARTESIAN_POINT('',(-0.0951557364069925,0.,0.));
#10141=MECHANICAL_DESIGN_GEOMETRIC_PRESENTATION_REPRESENTATION('',(#5562),#10142);
#10142=(
GEOMETRIC_REPRESENTATION_CONTEXT(3)
GLOBAL_UNCERTAINTY_ASSIGNED_CONTEXT((#10158))
GLOBAL_UNIT_ASSIGNED_CONTEXT((#10176,#10175,#10174))
REPRESENTATION_CONTEXT('MAS-674','TOP_LEVEL_ASSEMBLY_PART')
);
#10153=(
GEOMETRIC_REPRESENTATION_CONTEXT(3)
GLOBAL_UNCERTAINTY_ASSIGNED_CONTEXT((#10169))
GLOBAL_UNIT_ASSIGNED_CONTEXT((#10176,#10175,#10174))
REPRESENTATION_CONTEXT('Part 3','COMPONENT_PART')
);
#10158=UNCERTAINTY_MEASURE_WITH_UNIT(LENGTH_MEASURE(1.E-8),#10176,
'DISTANCE_ACCURACY_VALUE','Maximum Tolerance applied to model');
#10169=UNCERTAINTY_MEASURE_WITH_UNIT(LENGTH_MEASURE(2.E-5),#10176,
'DISTANCE_ACCURACY_VALUE','Maximum Tolerance applied to model');
#10174=(
NAMED_UNIT(*)
SI_UNIT($,.STERADIAN.)
SOLID_ANGLE_UNIT()
);
#10175=(
NAMED_UNIT(*)
PLANE_ANGLE_UNIT()
SI_UNIT($,.RADIAN.)
);
#10176=(
LENGTH_UNIT()
NAMED_UNIT(*)
SI_UNIT($,.METRE.)
);
#10199=PRODUCT_DEFINITION_SHAPE('','',#10221);
#10221=PRODUCT_DEFINITION('','',#10253,#10237);
#10237=PRODUCT_DEFINITION_CONTEXT('',#10323,'design');
#10253=PRODUCT_DEFINITION_FORMATION_WITH_SPECIFIED_SOURCE('','',#10285,
 .NOT_KNOWN.);
#10285=PRODUCT('Part 3','Part 3','Part 3',(#10317));
#10317=PRODUCT_CONTEXT('',#10323,'mechanical');
#10323=APPLICATION_CONTEXT('managed model based 3d engineering');
ENDSEC;
END-ISO-10303-21;
